ISO-10303-21;
HEADER;
/* Generated by software containing ST-Developer
 * from STEP Tools, Inc. (www.steptools.com) 
 */

FILE_DESCRIPTION(
/* description */ ('Guided pneumatic stop gate'),
/* implementation_level */ '2;1');

FILE_NAME(
/* name */ 'Cap Screw - M5x20.step',
/* time_stamp */ '2026-10-27T21:43:45-07:00',
/* author */ (''),
/* organization */ (''),
/* preprocessor_version */ 'ST-DEVELOPER v20.2',
/* originating_system */ 'Autodesk Translation Framework v15.17.0.0',
/* authorisation */ '');

FILE_SCHEMA (('AUTOMOTIVE_DESIGN { 1 0 10303 214 3 1 1 }'));
ENDSEC;

DATA;
#10=MECHANICAL_DESIGN_GEOMETRIC_PRESENTATION_REPRESENTATION('',(#545),#14392);
#415=ORIENTED_CLOSED_SHELL('',*,#7886,.F.);
#419=BREP_WITH_VOIDS('Body1',#7885,(#415));
#427=CONICAL_SURFACE('',#8700,0.4,0.785398163397448);
#428=CONICAL_SURFACE('',#8704,0.41,0.785398163397448);
#429=CONICAL_SURFACE('',#8708,0.26,0.463647609000806);
#430=CONICAL_SURFACE('',#8712,0.225,0.785398163397448);
#461=SHAPE_REPRESENTATION_RELATIONSHIP('SRR','None',#14595,#503);
#503=ADVANCED_BREP_SHAPE_REPRESENTATION('',(#419),#14357);
#545=STYLED_ITEM('',(#14898),#419);
#681=FACE_BOUND('',#1827,.T.);
#937=PLANE('',#8698);
#938=PLANE('',#8706);
#939=PLANE('',#8714);
#940=PLANE('',#8715);
#941=PLANE('',#8716);
#942=PLANE('',#8717);
#943=PLANE('',#8718);
#944=PLANE('',#8719);
#945=PLANE('',#8720);
#946=PLANE('',#8721);
#947=PLANE('',#8722);
#1281=FACE_OUTER_BOUND('',#1822,.T.);
#1282=FACE_OUTER_BOUND('',#1823,.T.);
#1283=FACE_OUTER_BOUND('',#1824,.T.);
#1284=FACE_OUTER_BOUND('',#1825,.T.);
#1285=FACE_OUTER_BOUND('',#1826,.T.);
#1286=FACE_OUTER_BOUND('',#1828,.T.);
#1287=FACE_OUTER_BOUND('',#1829,.T.);
#1288=FACE_OUTER_BOUND('',#1830,.T.);
#1289=FACE_OUTER_BOUND('',#1831,.T.);
#1290=FACE_OUTER_BOUND('',#1832,.T.);
#1291=FACE_OUTER_BOUND('',#1833,.T.);
#1292=FACE_OUTER_BOUND('',#1834,.T.);
#1293=FACE_OUTER_BOUND('',#1835,.T.);
#1294=FACE_OUTER_BOUND('',#1836,.T.);
#1295=FACE_OUTER_BOUND('',#1837,.T.);
#1296=FACE_OUTER_BOUND('',#1838,.T.);
#1297=FACE_OUTER_BOUND('',#1839,.T.);
#1822=EDGE_LOOP('',(#5970));
#1823=EDGE_LOOP('',(#5971,#5972,#5973,#5974));
#1824=EDGE_LOOP('',(#5975,#5976,#5977,#5978));
#1825=EDGE_LOOP('',(#5979,#5980,#5981,#5982));
#1826=EDGE_LOOP('',(#5983));
#1827=EDGE_LOOP('',(#5984));
#1828=EDGE_LOOP('',(#5985,#5986,#5987,#5988));
#1829=EDGE_LOOP('',(#5989,#5990,#5991,#5992));
#1830=EDGE_LOOP('',(#5993,#5994,#5995,#5996));
#1831=EDGE_LOOP('',(#5997));
#1832=EDGE_LOOP('',(#5998,#5999,#6000,#6001));
#1833=EDGE_LOOP('',(#6002,#6003,#6004,#6005));
#1834=EDGE_LOOP('',(#6006,#6007,#6008,#6009));
#1835=EDGE_LOOP('',(#6010,#6011,#6012,#6013));
#1836=EDGE_LOOP('',(#6014,#6015,#6016,#6017));
#1837=EDGE_LOOP('',(#6018,#6019,#6020,#6021));
#1838=EDGE_LOOP('',(#6022,#6023,#6024,#6025,#6026,#6027));
#1839=EDGE_LOOP('',(#6028,#6029,#6030,#6031,#6032,#6033));
#2467=LINE('',#12635,#3012);
#2468=LINE('',#12639,#3013);
#2469=LINE('',#12643,#3014);
#2470=LINE('',#12650,#3015);
#2471=LINE('',#12654,#3016);
#2472=LINE('',#12658,#3017);
#2473=LINE('',#12663,#3018);
#2474=LINE('',#12665,#3019);
#2475=LINE('',#12667,#3020);
#2476=LINE('',#12668,#3021);
#2477=LINE('',#12671,#3022);
#2478=LINE('',#12673,#3023);
#2479=LINE('',#12674,#3024);
#2480=LINE('',#12677,#3025);
#2481=LINE('',#12679,#3026);
#2482=LINE('',#12680,#3027);
#2483=LINE('',#12683,#3028);
#2484=LINE('',#12685,#3029);
#2485=LINE('',#12686,#3030);
#2486=LINE('',#12689,#3031);
#2487=LINE('',#12691,#3032);
#2488=LINE('',#12692,#3033);
#2489=LINE('',#12694,#3034);
#2490=LINE('',#12695,#3035);
#3012=VECTOR('',#10206,0.4);
#3013=VECTOR('',#10211,0.425);
#3014=VECTOR('',#10216,0.41);
#3015=VECTOR('',#10225,0.26);
#3016=VECTOR('',#10230,0.25);
#3017=VECTOR('',#10235,0.225);
#3018=VECTOR('',#10240,1.);
#3019=VECTOR('',#10241,1.);
#3020=VECTOR('',#10242,1.);
#3021=VECTOR('',#10243,1.);
#3022=VECTOR('',#10246,1.);
#3023=VECTOR('',#10247,1.);
#3024=VECTOR('',#10248,1.);
#3025=VECTOR('',#10251,1.);
#3026=VECTOR('',#10252,1.);
#3027=VECTOR('',#10253,1.);
#3028=VECTOR('',#10256,1.);
#3029=VECTOR('',#10257,1.);
#3030=VECTOR('',#10258,1.);
#3031=VECTOR('',#10261,1.);
#3032=VECTOR('',#10262,1.);
#3033=VECTOR('',#10263,1.);
#3034=VECTOR('',#10266,1.);
#3035=VECTOR('',#10267,1.);
#3492=CIRCLE('',#8699,0.375);
#3493=CIRCLE('',#8701,0.425);
#3494=CIRCLE('',#8703,0.425);
#3495=CIRCLE('',#8705,0.395);
#3496=CIRCLE('',#8707,0.27);
#3497=CIRCLE('',#8709,0.24505);
#3498=CIRCLE('',#8711,0.24505);
#3499=CIRCLE('',#8713,0.2);
#3943=VERTEX_POINT('',#12630);
#3944=VERTEX_POINT('',#12633);
#3945=VERTEX_POINT('',#12637);
#3946=VERTEX_POINT('',#12641);
#3947=VERTEX_POINT('',#12645);
#3948=VERTEX_POINT('',#12648);
#3949=VERTEX_POINT('',#12652);
#3950=VERTEX_POINT('',#12656);
#3951=VERTEX_POINT('',#12661);
#3952=VERTEX_POINT('',#12662);
#3953=VERTEX_POINT('',#12664);
#3954=VERTEX_POINT('',#12666);
#3955=VERTEX_POINT('',#12670);
#3956=VERTEX_POINT('',#12672);
#3957=VERTEX_POINT('',#12676);
#3958=VERTEX_POINT('',#12678);
#3959=VERTEX_POINT('',#12682);
#3960=VERTEX_POINT('',#12684);
#3961=VERTEX_POINT('',#12688);
#3962=VERTEX_POINT('',#12690);
#4683=EDGE_CURVE('',#3943,#3943,#3492,.T.);
#4684=EDGE_CURVE('',#3944,#3944,#3493,.T.);
#4685=EDGE_CURVE('',#3944,#3943,#2467,.T.);
#4686=EDGE_CURVE('',#3945,#3945,#3494,.T.);
#4687=EDGE_CURVE('',#3945,#3944,#2468,.T.);
#4688=EDGE_CURVE('',#3946,#3946,#3495,.T.);
#4689=EDGE_CURVE('',#3946,#3945,#2469,.T.);
#4690=EDGE_CURVE('',#3947,#3947,#3496,.T.);
#4691=EDGE_CURVE('',#3948,#3948,#3497,.F.);
#4692=EDGE_CURVE('',#3948,#3947,#2470,.T.);
#4693=EDGE_CURVE('',#3949,#3949,#3498,.F.);
#4694=EDGE_CURVE('',#3949,#3948,#2471,.T.);
#4695=EDGE_CURVE('',#3950,#3950,#3499,.T.);
#4696=EDGE_CURVE('',#3950,#3949,#2472,.T.);
#4697=EDGE_CURVE('',#3951,#3952,#2473,.T.);
#4698=EDGE_CURVE('',#3952,#3953,#2474,.T.);
#4699=EDGE_CURVE('',#3953,#3954,#2475,.T.);
#4700=EDGE_CURVE('',#3951,#3954,#2476,.T.);
#4701=EDGE_CURVE('',#3952,#3955,#2477,.T.);
#4702=EDGE_CURVE('',#3955,#3956,#2478,.T.);
#4703=EDGE_CURVE('',#3956,#3953,#2479,.T.);
#4704=EDGE_CURVE('',#3955,#3957,#2480,.T.);
#4705=EDGE_CURVE('',#3957,#3958,#2481,.T.);
#4706=EDGE_CURVE('',#3958,#3956,#2482,.T.);
#4707=EDGE_CURVE('',#3957,#3959,#2483,.T.);
#4708=EDGE_CURVE('',#3959,#3960,#2484,.T.);
#4709=EDGE_CURVE('',#3960,#3958,#2485,.T.);
#4710=EDGE_CURVE('',#3959,#3961,#2486,.T.);
#4711=EDGE_CURVE('',#3961,#3962,#2487,.T.);
#4712=EDGE_CURVE('',#3962,#3960,#2488,.T.);
#4713=EDGE_CURVE('',#3961,#3951,#2489,.T.);
#4714=EDGE_CURVE('',#3954,#3962,#2490,.T.);
#5970=ORIENTED_EDGE('',*,*,#4683,.F.);
#5971=ORIENTED_EDGE('',*,*,#4684,.F.);
#5972=ORIENTED_EDGE('',*,*,#4685,.T.);
#5973=ORIENTED_EDGE('',*,*,#4683,.T.);
#5974=ORIENTED_EDGE('',*,*,#4685,.F.);
#5975=ORIENTED_EDGE('',*,*,#4686,.F.);
#5976=ORIENTED_EDGE('',*,*,#4687,.T.);
#5977=ORIENTED_EDGE('',*,*,#4684,.T.);
#5978=ORIENTED_EDGE('',*,*,#4687,.F.);
#5979=ORIENTED_EDGE('',*,*,#4688,.F.);
#5980=ORIENTED_EDGE('',*,*,#4689,.T.);
#5981=ORIENTED_EDGE('',*,*,#4686,.T.);
#5982=ORIENTED_EDGE('',*,*,#4689,.F.);
#5983=ORIENTED_EDGE('',*,*,#4688,.T.);
#5984=ORIENTED_EDGE('',*,*,#4690,.F.);
#5985=ORIENTED_EDGE('',*,*,#4691,.F.);
#5986=ORIENTED_EDGE('',*,*,#4692,.T.);
#5987=ORIENTED_EDGE('',*,*,#4690,.T.);
#5988=ORIENTED_EDGE('',*,*,#4692,.F.);
#5989=ORIENTED_EDGE('',*,*,#4693,.F.);
#5990=ORIENTED_EDGE('',*,*,#4694,.T.);
#5991=ORIENTED_EDGE('',*,*,#4691,.T.);
#5992=ORIENTED_EDGE('',*,*,#4694,.F.);
#5993=ORIENTED_EDGE('',*,*,#4695,.F.);
#5994=ORIENTED_EDGE('',*,*,#4696,.T.);
#5995=ORIENTED_EDGE('',*,*,#4693,.T.);
#5996=ORIENTED_EDGE('',*,*,#4696,.F.);
#5997=ORIENTED_EDGE('',*,*,#4695,.T.);
#5998=ORIENTED_EDGE('',*,*,#4697,.T.);
#5999=ORIENTED_EDGE('',*,*,#4698,.T.);
#6000=ORIENTED_EDGE('',*,*,#4699,.T.);
#6001=ORIENTED_EDGE('',*,*,#4700,.F.);
#6002=ORIENTED_EDGE('',*,*,#4701,.T.);
#6003=ORIENTED_EDGE('',*,*,#4702,.T.);
#6004=ORIENTED_EDGE('',*,*,#4703,.T.);
#6005=ORIENTED_EDGE('',*,*,#4698,.F.);
#6006=ORIENTED_EDGE('',*,*,#4704,.T.);
#6007=ORIENTED_EDGE('',*,*,#4705,.T.);
#6008=ORIENTED_EDGE('',*,*,#4706,.T.);
#6009=ORIENTED_EDGE('',*,*,#4702,.F.);
#6010=ORIENTED_EDGE('',*,*,#4707,.T.);
#6011=ORIENTED_EDGE('',*,*,#4708,.T.);
#6012=ORIENTED_EDGE('',*,*,#4709,.T.);
#6013=ORIENTED_EDGE('',*,*,#4705,.F.);
#6014=ORIENTED_EDGE('',*,*,#4710,.T.);
#6015=ORIENTED_EDGE('',*,*,#4711,.T.);
#6016=ORIENTED_EDGE('',*,*,#4712,.T.);
#6017=ORIENTED_EDGE('',*,*,#4708,.F.);
#6018=ORIENTED_EDGE('',*,*,#4713,.T.);
#6019=ORIENTED_EDGE('',*,*,#4700,.T.);
#6020=ORIENTED_EDGE('',*,*,#4714,.T.);
#6021=ORIENTED_EDGE('',*,*,#4711,.F.);
#6022=ORIENTED_EDGE('',*,*,#4713,.F.);
#6023=ORIENTED_EDGE('',*,*,#4710,.F.);
#6024=ORIENTED_EDGE('',*,*,#4707,.F.);
#6025=ORIENTED_EDGE('',*,*,#4704,.F.);
#6026=ORIENTED_EDGE('',*,*,#4701,.F.);
#6027=ORIENTED_EDGE('',*,*,#4697,.F.);
#6028=ORIENTED_EDGE('',*,*,#4714,.F.);
#6029=ORIENTED_EDGE('',*,*,#4699,.F.);
#6030=ORIENTED_EDGE('',*,*,#4703,.F.);
#6031=ORIENTED_EDGE('',*,*,#4706,.F.);
#6032=ORIENTED_EDGE('',*,*,#4709,.F.);
#6033=ORIENTED_EDGE('',*,*,#4712,.F.);
#7297=CYLINDRICAL_SURFACE('',#8702,0.425);
#7298=CYLINDRICAL_SURFACE('',#8710,0.24505);
#7563=ADVANCED_FACE('',(#1281),#937,.T.);
#7564=ADVANCED_FACE('',(#1282),#427,.T.);
#7565=ADVANCED_FACE('',(#1283),#7297,.T.);
#7566=ADVANCED_FACE('',(#1284),#428,.T.);
#7567=ADVANCED_FACE('',(#1285,#681),#938,.T.);
#7568=ADVANCED_FACE('',(#1286),#429,.T.);
#7569=ADVANCED_FACE('',(#1287),#7298,.T.);
#7570=ADVANCED_FACE('',(#1288),#430,.T.);
#7571=ADVANCED_FACE('',(#1289),#939,.T.);
#7572=ADVANCED_FACE('',(#1290),#940,.F.);
#7573=ADVANCED_FACE('',(#1291),#941,.F.);
#7574=ADVANCED_FACE('',(#1292),#942,.F.);
#7575=ADVANCED_FACE('',(#1293),#943,.F.);
#7576=ADVANCED_FACE('',(#1294),#944,.F.);
#7577=ADVANCED_FACE('',(#1295),#945,.F.);
#7578=ADVANCED_FACE('',(#1296),#946,.F.);
#7579=ADVANCED_FACE('',(#1297),#947,.F.);
#7885=CLOSED_SHELL('',(#7563,#7564,#7565,#7566,#7567,#7568,#7569,#7570,
#7571));
#7886=CLOSED_SHELL('',(#7572,#7573,#7574,#7575,#7576,#7577,#7578,#7579));
#8697=AXIS2_PLACEMENT_3D('',#12628,#10196,#10197);
#8698=AXIS2_PLACEMENT_3D('',#12629,#10198,#10199);
#8699=AXIS2_PLACEMENT_3D('',#12631,#10200,#10201);
#8700=AXIS2_PLACEMENT_3D('',#12632,#10202,#10203);
#8701=AXIS2_PLACEMENT_3D('',#12634,#10204,#10205);
#8702=AXIS2_PLACEMENT_3D('',#12636,#10207,#10208);
#8703=AXIS2_PLACEMENT_3D('',#12638,#10209,#10210);
#8704=AXIS2_PLACEMENT_3D('',#12640,#10212,#10213);
#8705=AXIS2_PLACEMENT_3D('',#12642,#10214,#10215);
#8706=AXIS2_PLACEMENT_3D('',#12644,#10217,#10218);
#8707=AXIS2_PLACEMENT_3D('',#12646,#10219,#10220);
#8708=AXIS2_PLACEMENT_3D('',#12647,#10221,#10222);
#8709=AXIS2_PLACEMENT_3D('',#12649,#10223,#10224);
#8710=AXIS2_PLACEMENT_3D('',#12651,#10226,#10227);
#8711=AXIS2_PLACEMENT_3D('',#12653,#10228,#10229);
#8712=AXIS2_PLACEMENT_3D('',#12655,#10231,#10232);
#8713=AXIS2_PLACEMENT_3D('',#12657,#10233,#10234);
#8714=AXIS2_PLACEMENT_3D('',#12659,#10236,#10237);
#8715=AXIS2_PLACEMENT_3D('',#12660,#10238,#10239);
#8716=AXIS2_PLACEMENT_3D('',#12669,#10244,#10245);
#8717=AXIS2_PLACEMENT_3D('',#12675,#10249,#10250);
#8718=AXIS2_PLACEMENT_3D('',#12681,#10254,#10255);
#8719=AXIS2_PLACEMENT_3D('',#12687,#10259,#10260);
#8720=AXIS2_PLACEMENT_3D('',#12693,#10264,#10265);
#8721=AXIS2_PLACEMENT_3D('',#12696,#10268,#10269);
#8722=AXIS2_PLACEMENT_3D('',#12697,#10270,#10271);
#10196=DIRECTION('axis',(0.,0.,1.));
#10197=DIRECTION('refdir',(1.,0.,0.));
#10198=DIRECTION('center_axis',(0.,1.,0.));
#10199=DIRECTION('ref_axis',(0.,0.,1.));
#10200=DIRECTION('center_axis',(0.,-1.,0.));
#10201=DIRECTION('ref_axis',(1.,0.,0.));
#10202=DIRECTION('center_axis',(0.,-1.,0.));
#10203=DIRECTION('ref_axis',(1.,0.,0.));
#10204=DIRECTION('center_axis',(0.,-1.,0.));
#10205=DIRECTION('ref_axis',(1.,0.,0.));
#10206=DIRECTION('',(0.707106781186548,0.707106781186547,8.65956056235493E-17));
#10207=DIRECTION('center_axis',(0.,-1.,0.));
#10208=DIRECTION('ref_axis',(1.,0.,0.));
#10209=DIRECTION('center_axis',(0.,-1.,0.));
#10210=DIRECTION('ref_axis',(1.,0.,0.));
#10211=DIRECTION('',(0.,1.,0.));
#10212=DIRECTION('center_axis',(0.,1.,0.));
#10213=DIRECTION('ref_axis',(1.,0.,0.));
#10214=DIRECTION('center_axis',(0.,-1.,0.));
#10215=DIRECTION('ref_axis',(1.,0.,0.));
#10216=DIRECTION('',(-0.707106781186547,0.707106781186548,-8.65956056235493E-17));
#10217=DIRECTION('center_axis',(0.,-1.,0.));
#10218=DIRECTION('ref_axis',(0.,0.,-1.));
#10219=DIRECTION('center_axis',(0.,-1.,0.));
#10220=DIRECTION('ref_axis',(1.,0.,0.));
#10221=DIRECTION('center_axis',(0.,1.,0.));
#10222=DIRECTION('ref_axis',(1.,0.,0.));
#10223=DIRECTION('center_axis',(0.,1.,0.));
#10224=DIRECTION('ref_axis',(1.,0.,0.));
#10225=DIRECTION('',(-0.447213595499958,0.894427190999916,-5.47678698264203E-17));
#10226=DIRECTION('center_axis',(0.,-1.,0.));
#10227=DIRECTION('ref_axis',(1.,0.,0.));
#10228=DIRECTION('center_axis',(0.,1.,0.));
#10229=DIRECTION('ref_axis',(1.,0.,0.));
#10230=DIRECTION('',(0.,1.,0.));
#10231=DIRECTION('center_axis',(0.,1.,0.));
#10232=DIRECTION('ref_axis',(1.,0.,0.));
#10233=DIRECTION('center_axis',(0.,-1.,0.));
#10234=DIRECTION('ref_axis',(1.,0.,0.));
#10235=DIRECTION('',(-0.707106781186547,0.707106781186548,-8.65956056235493E-17));
#10236=DIRECTION('center_axis',(0.,-1.,0.));
#10237=DIRECTION('ref_axis',(0.,0.,-1.));
#10238=DIRECTION('center_axis',(0.866025403784439,0.,-0.5));
#10239=DIRECTION('ref_axis',(0.5,0.,0.866025403784439));
#10240=DIRECTION('',(-0.5,0.,-0.866025403784439));
#10241=DIRECTION('',(0.,-1.,0.));
#10242=DIRECTION('',(0.5,0.,0.866025403784439));
#10243=DIRECTION('',(0.,-1.,0.));
#10244=DIRECTION('center_axis',(1.20185167898973E-16,0.,-1.));
#10245=DIRECTION('ref_axis',(1.,0.,1.20185167898973E-16));
#10246=DIRECTION('',(-1.,0.,-1.20185167898973E-16));
#10247=DIRECTION('',(0.,-1.,0.));
#10248=DIRECTION('',(1.,0.,1.20185167898973E-16));
#10249=DIRECTION('center_axis',(-0.866025403784439,0.,-0.5));
#10250=DIRECTION('ref_axis',(0.5,0.,-0.866025403784439));
#10251=DIRECTION('',(-0.5,0.,0.866025403784439));
#10252=DIRECTION('',(0.,-1.,0.));
#10253=DIRECTION('',(0.5,0.,-0.866025403784439));
#10254=DIRECTION('center_axis',(-0.866025403784439,0.,0.5));
#10255=DIRECTION('ref_axis',(-0.5,0.,-0.866025403784439));
#10256=DIRECTION('',(0.5,0.,0.866025403784439));
#10257=DIRECTION('',(0.,-1.,0.));
#10258=DIRECTION('',(-0.5,0.,-0.866025403784439));
#10259=DIRECTION('center_axis',(-2.40370335797945E-16,0.,1.));
#10260=DIRECTION('ref_axis',(-1.,0.,-2.40370335797945E-16));
#10261=DIRECTION('',(1.,0.,2.40370335797945E-16));
#10262=DIRECTION('',(0.,-1.,0.));
#10263=DIRECTION('',(-1.,0.,-2.40370335797945E-16));
#10264=DIRECTION('center_axis',(0.866025403784439,0.,0.5));
#10265=DIRECTION('ref_axis',(-0.5,0.,0.866025403784439));
#10266=DIRECTION('',(0.5,0.,-0.866025403784439));
#10267=DIRECTION('',(-0.5,0.,0.866025403784439));
#10268=DIRECTION('center_axis',(0.,1.,0.));
#10269=DIRECTION('ref_axis',(1.,0.,0.));
#10270=DIRECTION('center_axis',(0.,-1.,0.));
#10271=DIRECTION('ref_axis',(0.,0.,-1.));
#12628=CARTESIAN_POINT('',(0.,0.,0.));
#12629=CARTESIAN_POINT('Origin',(0.375,0.5,0.));
#12630=CARTESIAN_POINT('',(-0.375,0.5,-4.59242549680257E-17));
#12631=CARTESIAN_POINT('Origin',(0.,0.5,0.));
#12632=CARTESIAN_POINT('Origin',(0.,0.475,0.));
#12633=CARTESIAN_POINT('',(-0.425,0.45,-5.20474889637625E-17));
#12634=CARTESIAN_POINT('Origin',(0.,0.45,0.));
#12635=CARTESIAN_POINT('',(-0.4,0.475,-4.89858719658941E-17));
#12636=CARTESIAN_POINT('Origin',(0.,0.24,0.));
#12637=CARTESIAN_POINT('',(-0.425,0.0299999999999998,-5.20474889637625E-17));
#12638=CARTESIAN_POINT('Origin',(0.,0.0299999999999998,0.));
#12639=CARTESIAN_POINT('',(-0.425,0.24,-5.20474889637625E-17));
#12640=CARTESIAN_POINT('Origin',(0.,0.0150000000000001,0.));
#12641=CARTESIAN_POINT('',(-0.395,4.85722573273506E-17,-4.83735485663204E-17));
#12642=CARTESIAN_POINT('Origin',(0.,0.,0.));
#12643=CARTESIAN_POINT('',(-0.41,0.0150000000000001,-5.02105187650415E-17));
#12644=CARTESIAN_POINT('Origin',(0.27,0.,0.));
#12645=CARTESIAN_POINT('',(-0.27,0.,-3.30654635769785E-17));
#12646=CARTESIAN_POINT('Origin',(0.,0.,0.));
#12647=CARTESIAN_POINT('Origin',(0.,-0.02,0.));
#12648=CARTESIAN_POINT('',(-0.24505,-0.0498999999999999,3.00099698131059E-17));
#12649=CARTESIAN_POINT('Origin',(0.,-0.0498999999999999,0.));
#12650=CARTESIAN_POINT('',(-0.26,-0.02,-3.18408167778312E-17));
#12651=CARTESIAN_POINT('Origin',(0.,-0.995,0.));
#12652=CARTESIAN_POINT('',(-0.24505,-1.95495,3.00099698131059E-17));
#12653=CARTESIAN_POINT('Origin',(0.,-1.95495,0.));
#12654=CARTESIAN_POINT('',(-0.24505,-0.995,-3.00099698131059E-17));
#12655=CARTESIAN_POINT('Origin',(0.,-1.975,0.));
#12656=CARTESIAN_POINT('',(-0.2,-2.,-2.44929359829471E-17));
#12657=CARTESIAN_POINT('Origin',(0.,-2.,0.));
#12658=CARTESIAN_POINT('',(-0.225,-1.975,-2.75545529808154E-17));
#12659=CARTESIAN_POINT('Origin',(0.,-2.,0.));
#12660=CARTESIAN_POINT('Origin',(0.115470053837925,-0.5,-0.2));
#12661=CARTESIAN_POINT('',(0.23094010767585,-0.5,0.));
#12662=CARTESIAN_POINT('',(0.115470053837925,-0.5,-0.2));
#12663=CARTESIAN_POINT('',(0.23094010767585,-0.5,0.));
#12664=CARTESIAN_POINT('',(0.115470053837925,-0.8,-0.2));
#12665=CARTESIAN_POINT('',(0.115470053837925,-0.5,-0.2));
#12666=CARTESIAN_POINT('',(0.23094010767585,-0.8,0.));
#12667=CARTESIAN_POINT('',(0.23094010767585,-0.8,0.));
#12668=CARTESIAN_POINT('',(0.23094010767585,-0.5,0.));
#12669=CARTESIAN_POINT('Origin',(-0.115470053837925,-0.5,-0.2));
#12670=CARTESIAN_POINT('',(-0.115470053837925,-0.5,-0.2));
#12671=CARTESIAN_POINT('',(0.115470053837925,-0.5,-0.2));
#12672=CARTESIAN_POINT('',(-0.115470053837925,-0.8,-0.2));
#12673=CARTESIAN_POINT('',(-0.115470053837925,-0.5,-0.2));
#12674=CARTESIAN_POINT('',(0.115470053837925,-0.8,-0.2));
#12675=CARTESIAN_POINT('Origin',(-0.23094010767585,-0.5,-2.77555756156289E-17));
#12676=CARTESIAN_POINT('',(-0.23094010767585,-0.5,-2.82820063659975E-17));
#12677=CARTESIAN_POINT('',(-0.115470053837925,-0.5,-0.2));
#12678=CARTESIAN_POINT('',(-0.23094010767585,-0.8,-2.77555756156289E-17));
#12679=CARTESIAN_POINT('',(-0.23094010767585,-0.5,-2.82820063659975E-17));
#12680=CARTESIAN_POINT('',(-0.115470053837925,-0.8,-0.2));
#12681=CARTESIAN_POINT('Origin',(-0.115470053837925,-0.5,0.2));
#12682=CARTESIAN_POINT('',(-0.115470053837925,-0.5,0.2));
#12683=CARTESIAN_POINT('',(-0.23094010767585,-0.5,-2.82820063659975E-17));
#12684=CARTESIAN_POINT('',(-0.115470053837925,-0.8,0.2));
#12685=CARTESIAN_POINT('',(-0.115470053837925,-0.5,0.2));
#12686=CARTESIAN_POINT('',(-0.23094010767585,-0.8,-2.82820063659975E-17));
#12687=CARTESIAN_POINT('Origin',(0.115470053837925,-0.5,0.2));
#12688=CARTESIAN_POINT('',(0.115470053837925,-0.5,0.2));
#12689=CARTESIAN_POINT('',(-0.115470053837925,-0.5,0.2));
#12690=CARTESIAN_POINT('',(0.115470053837925,-0.8,0.2));
#12691=CARTESIAN_POINT('',(0.115470053837925,-0.5,0.2));
#12692=CARTESIAN_POINT('',(-0.115470053837925,-0.8,0.2));
#12693=CARTESIAN_POINT('Origin',(0.23094010767585,-0.5,0.));
#12694=CARTESIAN_POINT('',(0.115470053837925,-0.5,0.2));
#12695=CARTESIAN_POINT('',(0.115470053837925,-0.8,0.2));
#12696=CARTESIAN_POINT('Origin',(0.,-0.5,0.));
#12697=CARTESIAN_POINT('Origin',(0.,-0.8,0.));
#14309=UNCERTAINTY_MEASURE_WITH_UNIT(LENGTH_MEASURE(0.001),#14393,
'DISTANCE_ACCURACY_VALUE',
'Maximum model space distance between geometric entities at asserted c
onnectivities');
#14344=UNCERTAINTY_MEASURE_WITH_UNIT(LENGTH_MEASURE(0.001),#14393,
'DISTANCE_ACCURACY_VALUE',
'Maximum model space distance between geometric entities at asserted c
onnectivities');
#14357=(
GEOMETRIC_REPRESENTATION_CONTEXT(3)
GLOBAL_UNCERTAINTY_ASSIGNED_CONTEXT((#14309))
GLOBAL_UNIT_ASSIGNED_CONTEXT((#14393,#14395,#14396))
REPRESENTATION_CONTEXT('','3D')
);
#14392=(
GEOMETRIC_REPRESENTATION_CONTEXT(3)
GLOBAL_UNCERTAINTY_ASSIGNED_CONTEXT((#14344))
GLOBAL_UNIT_ASSIGNED_CONTEXT((#14393,#14395,#14396))
REPRESENTATION_CONTEXT('','3D')
);
#14393=(
LENGTH_UNIT()
NAMED_UNIT(*)
SI_UNIT(.CENTI.,.METRE.)
);
#14395=(
NAMED_UNIT(*)
PLANE_ANGLE_UNIT()
SI_UNIT($,.RADIAN.)
);
#14396=(
NAMED_UNIT(*)
SI_UNIT($,.STERADIAN.)
SOLID_ANGLE_UNIT()
);
#14409=SHAPE_DEFINITION_REPRESENTATION(#14456,#14595);
#14456=PRODUCT_DEFINITION_SHAPE('',$,#14643);
#14595=SHAPE_REPRESENTATION('',(#8697),#14357);
#14630=PRODUCT_DEFINITION_CONTEXT('part definition',#14773,'design');
#14643=PRODUCT_DEFINITION('Cap Screw - M5x20','Cap Screw - M5x20',#14690,
#14630);
#14690=PRODUCT_DEFINITION_FORMATION('',$,#14787);
#14773=APPLICATION_CONTEXT(
'Core Data for Automotive Mechanical Design Process');
#14774=PRODUCT_CONTEXT('part definition',#14773,'mechanical');
#14787=PRODUCT('Cap Screw - M5x20','Cap Screw - M5x20',
'Cap Screw - M5x20',(#14774));
#14892=COLOUR_RGB('Black',0.12,0.14,0.17);
#14893=FILL_AREA_STYLE_COLOUR('',#14892);
#14894=FILL_AREA_STYLE('',(#14893));
#14895=SURFACE_STYLE_FILL_AREA(#14894);
#14896=SURFACE_SIDE_STYLE('',(#14895));
#14897=SURFACE_STYLE_USAGE(.BOTH.,#14896);
#14898=PRESENTATION_STYLE_ASSIGNMENT((#14897));
ENDSEC;
END-ISO-10303-21;
